ISO-10303-21;
HEADER;
FILE_DESCRIPTION((''),'2;1');
FILE_NAME('Clamp_Bolt_2.step','2026-10-09T10:15:02-07:00',(''),(''),'','','');
FILE_SCHEMA (('AUTOMOTIVE_DESIGN { 1 0 10303 214 3 1 1 }'));
ENDSEC;
DATA;
#10=MECHANICAL_DESIGN_GEOMETRIC_PRESENTATION_REPRESENTATION('',(#90),#6779);
#53=TOROIDAL_SURFACE('',#4367,4.4,0.6) ;
#54=TOROIDAL_SURFACE('',#4371,3.25,0.25) ;
#70=SHAPE_REPRESENTATION_RELATIONSHIP('SRR','None',#6824,#80) ;
#80=ADVANCED_BREP_SHAPE_REPRESENTATION('',(#100),#6776) ;
#90=STYLED_ITEM('',(#6877),#100) ;
#100=MANIFOLD_SOLID_BREP('Body1',#3902) ;
#129=FACE_BOUND('',#804,.T.) ;
#130=FACE_BOUND('',#806,.T.) ;
#233=PLANE('',#4353) ;
#234=PLANE('',#4354) ;
#235=PLANE('',#4355) ;
#236=PLANE('',#4356) ;
#237=PLANE('',#4357) ;
#238=PLANE('',#4358) ;
#239=PLANE('',#4359) ;
#240=PLANE('',#4360) ;
#241=PLANE('',#4362) ;
#242=PLANE('',#4365) ;
#324=CONICAL_SURFACE('',#4376,2.5,0.785398163397) ;
#526=FACE_OUTER_BOUND('',#796,.T.) ;
#527=FACE_OUTER_BOUND('',#797,.T.) ;
#528=FACE_OUTER_BOUND('',#798,.T.) ;
#529=FACE_OUTER_BOUND('',#799,.T.) ;
#530=FACE_OUTER_BOUND('',#800,.T.) ;
#531=FACE_OUTER_BOUND('',#801,.T.) ;
#532=FACE_OUTER_BOUND('',#802,.T.) ;
#533=FACE_OUTER_BOUND('',#803,.T.) ;
#534=FACE_OUTER_BOUND('',#805,.T.) ;
#535=FACE_OUTER_BOUND('',#807,.T.) ;
#536=FACE_OUTER_BOUND('',#808,.T.) ;
#537=FACE_OUTER_BOUND('',#809,.T.) ;
#538=FACE_OUTER_BOUND('',#810,.T.) ;
#539=FACE_OUTER_BOUND('',#811,.T.) ;
#540=FACE_OUTER_BOUND('',#812,.T.) ;
#796=EDGE_LOOP('',(#3423,#3424,#3425,#3426)) ;
#797=EDGE_LOOP('',(#3427,#3428,#3429,#3430)) ;
#798=EDGE_LOOP('',(#3431,#3432,#3433,#3434)) ;
#799=EDGE_LOOP('',(#3435,#3436,#3437,#3438,#3439,#3440)) ;
#800=EDGE_LOOP('',(#3441,#3442,#3443,#3444)) ;
#801=EDGE_LOOP('',(#3445,#3446,#3447,#3448)) ;
#802=EDGE_LOOP('',(#3449,#3450,#3451,#3452)) ;
#803=EDGE_LOOP('',(#3453)) ;
#804=EDGE_LOOP('',(#3454,#3455,#3456,#3457,#3458,#3459)) ;
#805=EDGE_LOOP('',(#3460)) ;
#806=EDGE_LOOP('',(#3461)) ;
#807=EDGE_LOOP('',(#3462)) ;
#808=EDGE_LOOP('',(#3463,#3464,#3465,#3466)) ;
#809=EDGE_LOOP('',(#3467,#3468,#3469,#3470)) ;
#810=EDGE_LOOP('',(#3471,#3472,#3473,#3474)) ;
#811=EDGE_LOOP('',(#3475,#3476,#3477,#3478)) ;
#812=EDGE_LOOP('',(#3479,#3480,#3481,#3482)) ;
#1144=LINE('',#6555,#1504) ;
#1145=LINE('',#6557,#1505) ;
#1146=LINE('',#6559,#1506) ;
#1147=LINE('',#6560,#1507) ;
#1148=LINE('',#6564,#1508) ;
#1149=LINE('',#6565,#1509) ;
#1150=LINE('',#6566,#1510) ;
#1151=LINE('',#6569,#1511) ;
#1152=LINE('',#6571,#1512) ;
#1153=LINE('',#6572,#1513) ;
#1154=LINE('',#6575,#1514) ;
#1155=LINE('',#6577,#1515) ;
#1156=LINE('',#6578,#1516) ;
#1157=LINE('',#6581,#1517) ;
#1158=LINE('',#6582,#1518) ;
#1159=LINE('',#6585,#1519) ;
#1160=LINE('',#6586,#1520) ;
#1161=LINE('',#6588,#1521) ;
#1162=LINE('',#6605,#1522) ;
#1163=LINE('',#6612,#1523) ;
#1164=LINE('',#6615,#1524) ;
#1504=VECTOR('',#5410,1.) ;
#1505=VECTOR('',#5411,1.) ;
#1506=VECTOR('',#5412,1.) ;
#1507=VECTOR('',#5413,1.) ;
#1508=VECTOR('',#5416,1.) ;
#1509=VECTOR('',#5417,0.99999999999962) ;
#1510=VECTOR('',#5418,0.99999999999962) ;
#1511=VECTOR('',#5421,0.99999999999962) ;
#1512=VECTOR('',#5422,1.) ;
#1513=VECTOR('',#5423,0.99999999999962) ;
#1514=VECTOR('',#5426,0.99999999999962) ;
#1515=VECTOR('',#5427,1.) ;
#1516=VECTOR('',#5428,0.99999999999962) ;
#1517=VECTOR('',#5431,1.) ;
#1518=VECTOR('',#5432,0.99999999999962) ;
#1519=VECTOR('',#5435,0.99999999999962) ;
#1520=VECTOR('',#5436,1.) ;
#1521=VECTOR('',#5439,1.) ;
#1522=VECTOR('',#5462,5.) ;
#1523=VECTOR('',#5471,3.) ;
#1524=VECTOR('',#5476,2.5) ;
#1696=CIRCLE('',#4361,4.4) ;
#1697=CIRCLE('',#4363,5.) ;
#1698=CIRCLE('',#4364,3.25) ;
#1699=CIRCLE('',#4366,2.5) ;
#1700=CIRCLE('',#4368,0.6) ;
#1701=CIRCLE('',#4369,5.) ;
#1702=CIRCLE('',#4372,0.25) ;
#1703=CIRCLE('',#4373,3.) ;
#1704=CIRCLE('',#4375,3.) ;
#1974=VERTEX_POINT('',#6553) ;
#1975=VERTEX_POINT('',#6554) ;
#1976=VERTEX_POINT('',#6556) ;
#1977=VERTEX_POINT('',#6558) ;
#1978=VERTEX_POINT('',#6562) ;
#1979=VERTEX_POINT('',#6563) ;
#1980=VERTEX_POINT('',#6568) ;
#1981=VERTEX_POINT('',#6570) ;
#1982=VERTEX_POINT('',#6574) ;
#1983=VERTEX_POINT('',#6576) ;
#1984=VERTEX_POINT('',#6580) ;
#1985=VERTEX_POINT('',#6584) ;
#1986=VERTEX_POINT('',#6590) ;
#1987=VERTEX_POINT('',#6593) ;
#1988=VERTEX_POINT('',#6595) ;
#1989=VERTEX_POINT('',#6598) ;
#1990=VERTEX_POINT('',#6601) ;
#1991=VERTEX_POINT('',#6607) ;
#1992=VERTEX_POINT('',#6611) ;
#2465=EDGE_CURVE('',#1974,#1975,#1144,.T.) ;
#2466=EDGE_CURVE('',#1974,#1976,#1145,.T.) ;
#2467=EDGE_CURVE('',#1976,#1977,#1146,.T.) ;
#2468=EDGE_CURVE('',#1975,#1977,#1147,.T.) ;
#2469=EDGE_CURVE('',#1978,#1979,#1148,.T.) ;
#2470=EDGE_CURVE('',#1978,#1974,#1149,.T.) ;
#2471=EDGE_CURVE('',#1979,#1975,#1150,.T.) ;
#2472=EDGE_CURVE('',#1976,#1980,#1151,.T.) ;
#2473=EDGE_CURVE('',#1980,#1981,#1152,.T.) ;
#2474=EDGE_CURVE('',#1977,#1981,#1153,.T.) ;
#2475=EDGE_CURVE('',#1981,#1982,#1154,.T.) ;
#2476=EDGE_CURVE('',#1982,#1983,#1155,.T.) ;
#2477=EDGE_CURVE('',#1983,#1979,#1156,.T.) ;
#2478=EDGE_CURVE('',#1984,#1983,#1157,.T.) ;
#2479=EDGE_CURVE('',#1984,#1978,#1158,.T.) ;
#2480=EDGE_CURVE('',#1980,#1985,#1159,.T.) ;
#2481=EDGE_CURVE('',#1985,#1982,#1160,.T.) ;
#2482=EDGE_CURVE('',#1985,#1984,#1161,.T.) ;
#2483=EDGE_CURVE('',#1986,#1986,#1696,.T.) ;
#2484=EDGE_CURVE('',#1987,#1987,#1697,.T.) ;
#2485=EDGE_CURVE('',#1988,#1988,#1698,.T.) ;
#2486=EDGE_CURVE('',#1989,#1989,#1699,.T.) ;
#2487=EDGE_CURVE('',#1986,#1990,#1700,.T.) ;
#2488=EDGE_CURVE('',#1990,#1990,#1701,.T.) ;
#2489=EDGE_CURVE('',#1990,#1987,#1162,.T.) ;
#2490=EDGE_CURVE('',#1988,#1991,#1702,.T.) ;
#2491=EDGE_CURVE('',#1991,#1991,#1703,.T.) ;
#2492=EDGE_CURVE('',#1991,#1992,#1163,.T.) ;
#2493=EDGE_CURVE('',#1992,#1992,#1704,.T.) ;
#2494=EDGE_CURVE('',#1992,#1989,#1164,.T.) ;
#3423=ORIENTED_EDGE('',*,*,#2465,.F.) ;
#3424=ORIENTED_EDGE('',*,*,#2466,.T.) ;
#3425=ORIENTED_EDGE('',*,*,#2467,.T.) ;
#3426=ORIENTED_EDGE('',*,*,#2468,.F.) ;
#3427=ORIENTED_EDGE('',*,*,#2469,.F.) ;
#3428=ORIENTED_EDGE('',*,*,#2470,.T.) ;
#3429=ORIENTED_EDGE('',*,*,#2465,.T.) ;
#3430=ORIENTED_EDGE('',*,*,#2471,.F.) ;
#3431=ORIENTED_EDGE('',*,*,#2467,.F.) ;
#3432=ORIENTED_EDGE('',*,*,#2472,.T.) ;
#3433=ORIENTED_EDGE('',*,*,#2473,.T.) ;
#3434=ORIENTED_EDGE('',*,*,#2474,.F.) ;
#3435=ORIENTED_EDGE('',*,*,#2468,.T.) ;
#3436=ORIENTED_EDGE('',*,*,#2474,.T.) ;
#3437=ORIENTED_EDGE('',*,*,#2475,.T.) ;
#3438=ORIENTED_EDGE('',*,*,#2476,.T.) ;
#3439=ORIENTED_EDGE('',*,*,#2477,.T.) ;
#3440=ORIENTED_EDGE('',*,*,#2471,.T.) ;
#3441=ORIENTED_EDGE('',*,*,#2478,.F.) ;
#3442=ORIENTED_EDGE('',*,*,#2479,.T.) ;
#3443=ORIENTED_EDGE('',*,*,#2469,.T.) ;
#3444=ORIENTED_EDGE('',*,*,#2477,.F.) ;
#3445=ORIENTED_EDGE('',*,*,#2473,.F.) ;
#3446=ORIENTED_EDGE('',*,*,#2480,.T.) ;
#3447=ORIENTED_EDGE('',*,*,#2481,.T.) ;
#3448=ORIENTED_EDGE('',*,*,#2475,.F.) ;
#3449=ORIENTED_EDGE('',*,*,#2481,.F.) ;
#3450=ORIENTED_EDGE('',*,*,#2482,.T.) ;
#3451=ORIENTED_EDGE('',*,*,#2478,.T.) ;
#3452=ORIENTED_EDGE('',*,*,#2476,.F.) ;
#3453=ORIENTED_EDGE('',*,*,#2483,.T.) ;
#3454=ORIENTED_EDGE('',*,*,#2479,.F.) ;
#3455=ORIENTED_EDGE('',*,*,#2482,.F.) ;
#3456=ORIENTED_EDGE('',*,*,#2480,.F.) ;
#3457=ORIENTED_EDGE('',*,*,#2472,.F.) ;
#3458=ORIENTED_EDGE('',*,*,#2466,.F.) ;
#3459=ORIENTED_EDGE('',*,*,#2470,.F.) ;
#3460=ORIENTED_EDGE('',*,*,#2484,.F.) ;
#3461=ORIENTED_EDGE('',*,*,#2485,.T.) ;
#3462=ORIENTED_EDGE('',*,*,#2486,.F.) ;
#3463=ORIENTED_EDGE('',*,*,#2483,.F.) ;
#3464=ORIENTED_EDGE('',*,*,#2487,.T.) ;
#3465=ORIENTED_EDGE('',*,*,#2488,.T.) ;
#3466=ORIENTED_EDGE('',*,*,#2487,.F.) ;
#3467=ORIENTED_EDGE('',*,*,#2488,.F.) ;
#3468=ORIENTED_EDGE('',*,*,#2489,.T.) ;
#3469=ORIENTED_EDGE('',*,*,#2484,.T.) ;
#3470=ORIENTED_EDGE('',*,*,#2489,.F.) ;
#3471=ORIENTED_EDGE('',*,*,#2485,.F.) ;
#3472=ORIENTED_EDGE('',*,*,#2490,.T.) ;
#3473=ORIENTED_EDGE('',*,*,#2491,.T.) ;
#3474=ORIENTED_EDGE('',*,*,#2490,.F.) ;
#3475=ORIENTED_EDGE('',*,*,#2491,.F.) ;
#3476=ORIENTED_EDGE('',*,*,#2492,.T.) ;
#3477=ORIENTED_EDGE('',*,*,#2493,.T.) ;
#3478=ORIENTED_EDGE('',*,*,#2492,.F.) ;
#3479=ORIENTED_EDGE('',*,*,#2493,.F.) ;
#3480=ORIENTED_EDGE('',*,*,#2494,.T.) ;
#3481=ORIENTED_EDGE('',*,*,#2486,.T.) ;
#3482=ORIENTED_EDGE('',*,*,#2494,.F.) ;
#3645=CYLINDRICAL_SURFACE('',#4370,5.) ;
#3646=CYLINDRICAL_SURFACE('',#4374,3.) ;
#3850=ADVANCED_FACE('',(#526),#233,.T.) ;
#3851=ADVANCED_FACE('',(#527),#234,.T.) ;
#3852=ADVANCED_FACE('',(#528),#235,.T.) ;
#3853=ADVANCED_FACE('',(#529),#236,.T.) ;
#3854=ADVANCED_FACE('',(#530),#237,.T.) ;
#3855=ADVANCED_FACE('',(#531),#238,.T.) ;
#3856=ADVANCED_FACE('',(#532),#239,.T.) ;
#3857=ADVANCED_FACE('',(#533,#129),#240,.T.) ;
#3858=ADVANCED_FACE('',(#534,#130),#241,.F.) ;
#3859=ADVANCED_FACE('',(#535),#242,.F.) ;
#3860=ADVANCED_FACE('',(#536),#53,.T.) ;
#3861=ADVANCED_FACE('',(#537),#3645,.T.) ;
#3862=ADVANCED_FACE('',(#538),#54,.F.) ;
#3863=ADVANCED_FACE('',(#539),#3646,.T.) ;
#3864=ADVANCED_FACE('',(#540),#324,.T.) ;
#3902=CLOSED_SHELL('',(#3850,#3851,#3852,#3853,#3854,#3855,#3856,#3857,
#3858,#3859,#3860,#3861,#3862,#3863,#3864)) ;
#4352=AXIS2_PLACEMENT_3D('',#6551,#5406,#5407) ;
#4353=AXIS2_PLACEMENT_3D('',#6552,#5408,#5409) ;
#4354=AXIS2_PLACEMENT_3D('',#6561,#5414,#5415) ;
#4355=AXIS2_PLACEMENT_3D('',#6567,#5419,#5420) ;
#4356=AXIS2_PLACEMENT_3D('',#6573,#5424,#5425) ;
#4357=AXIS2_PLACEMENT_3D('',#6579,#5429,#5430) ;
#4358=AXIS2_PLACEMENT_3D('',#6583,#5433,#5434) ;
#4359=AXIS2_PLACEMENT_3D('',#6587,#5437,#5438) ;
#4360=AXIS2_PLACEMENT_3D('',#6589,#5440,#5441) ;
#4361=AXIS2_PLACEMENT_3D('',#6591,#5442,#5443) ;
#4362=AXIS2_PLACEMENT_3D('',#6592,#5444,#5445) ;
#4363=AXIS2_PLACEMENT_3D('',#6594,#5446,#5447) ;
#4364=AXIS2_PLACEMENT_3D('',#6596,#5448,#5449) ;
#4365=AXIS2_PLACEMENT_3D('',#6597,#5450,#5451) ;
#4366=AXIS2_PLACEMENT_3D('',#6599,#5452,#5453) ;
#4367=AXIS2_PLACEMENT_3D('',#6600,#5454,#5455) ;
#4368=AXIS2_PLACEMENT_3D('',#6602,#5456,#5457) ;
#4369=AXIS2_PLACEMENT_3D('',#6603,#5458,#5459) ;
#4370=AXIS2_PLACEMENT_3D('',#6604,#5460,#5461) ;
#4371=AXIS2_PLACEMENT_3D('',#6606,#5463,#5464) ;
#4372=AXIS2_PLACEMENT_3D('',#6608,#5465,#5466) ;
#4373=AXIS2_PLACEMENT_3D('',#6609,#5467,#5468) ;
#4374=AXIS2_PLACEMENT_3D('',#6610,#5469,#5470) ;
#4375=AXIS2_PLACEMENT_3D('',#6613,#5472,#5473) ;
#4376=AXIS2_PLACEMENT_3D('',#6614,#5474,#5475) ;
#5406=DIRECTION('axis',(0.,0.,1.)) ;
#5407=DIRECTION('refdir',(1.,0.,0.)) ;
#5408=DIRECTION('center_axis',(1.,0.,-1.53837014911E-16)) ;
#5409=DIRECTION('ref_axis',(-1.53837014911E-16,0.,-1.)) ;
#5410=DIRECTION('',(0.,1.,0.)) ;
#5411=DIRECTION('',(0.,0.,-1.)) ;
#5412=DIRECTION('',(0.,1.,0.)) ;
#5413=DIRECTION('',(0.,0.,-1.)) ;
#5414=DIRECTION('center_axis',(0.50000000000019,0.,-0.866025403784329)) ;
#5415=DIRECTION('ref_axis',(-0.866025403784329,0.,-0.50000000000019)) ;
#5416=DIRECTION('',(0.,1.,0.)) ;
#5417=DIRECTION('',(-0.866025403784329,0.,-0.50000000000019)) ;
#5418=DIRECTION('',(-0.866025403784329,0.,-0.50000000000019)) ;
#5419=DIRECTION('center_axis',(0.50000000000019,0.,0.866025403784329)) ;
#5420=DIRECTION('ref_axis',(0.866025403784329,0.,-0.50000000000019)) ;
#5421=DIRECTION('',(0.866025403784329,0.,-0.50000000000019)) ;
#5422=DIRECTION('',(0.,1.,0.)) ;
#5423=DIRECTION('',(0.866025403784329,0.,-0.50000000000019)) ;
#5424=DIRECTION('center_axis',(0.,-1.,0.)) ;
#5425=DIRECTION('ref_axis',(1.,0.,0.)) ;
#5426=DIRECTION('',(0.866025403784329,0.,0.50000000000019)) ;
#5427=DIRECTION('',(0.,0.,1.)) ;
#5428=DIRECTION('',(-0.866025403784329,0.,0.50000000000019)) ;
#5429=DIRECTION('center_axis',(-0.50000000000019,0.,-0.866025403784329)) ;
#5430=DIRECTION('ref_axis',(-0.866025403784329,0.,0.50000000000019)) ;
#5431=DIRECTION('',(0.,1.,0.)) ;
#5432=DIRECTION('',(-0.866025403784329,0.,0.50000000000019)) ;
#5433=DIRECTION('center_axis',(-0.50000000000019,0.,0.866025403784329)) ;
#5434=DIRECTION('ref_axis',(0.866025403784329,0.,0.50000000000019)) ;
#5435=DIRECTION('',(0.866025403784329,0.,0.50000000000019)) ;
#5436=DIRECTION('',(0.,1.,0.)) ;
#5437=DIRECTION('center_axis',(-1.,0.,0.)) ;
#5438=DIRECTION('ref_axis',(0.,0.,1.)) ;
#5439=DIRECTION('',(0.,0.,1.)) ;
#5440=DIRECTION('center_axis',(0.,-1.,0.)) ;
#5441=DIRECTION('ref_axis',(-1.,0.,0.)) ;
#5442=DIRECTION('center_axis',(0.,-1.,0.)) ;
#5443=DIRECTION('ref_axis',(0.,0.,1.)) ;
#5444=DIRECTION('center_axis',(0.,-1.,0.)) ;
#5445=DIRECTION('ref_axis',(-1.,0.,0.)) ;
#5446=DIRECTION('center_axis',(0.,-1.,0.)) ;
#5447=DIRECTION('ref_axis',(0.,0.,1.)) ;
#5448=DIRECTION('center_axis',(0.,-1.,0.)) ;
#5449=DIRECTION('ref_axis',(0.,0.,1.)) ;
#5450=DIRECTION('center_axis',(0.,-1.,0.)) ;
#5451=DIRECTION('ref_axis',(-1.,0.,0.)) ;
#5452=DIRECTION('center_axis',(0.,-1.,0.)) ;
#5453=DIRECTION('ref_axis',(0.,0.,1.)) ;
#5454=DIRECTION('center_axis',(0.,-1.,0.)) ;
#5455=DIRECTION('ref_axis',(0.479425538604205,0.,-0.877582561890372)) ;
#5456=DIRECTION('center_axis',(-0.877582561890372,0.,-0.479425538604205)) ;
#5457=DIRECTION('ref_axis',(-0.479425538604205,0.,0.877582561890372)) ;
#5458=DIRECTION('center_axis',(0.,-1.,0.)) ;
#5459=DIRECTION('ref_axis',(0.,0.,1.)) ;
#5460=DIRECTION('center_axis',(0.,-1.,0.)) ;
#5461=DIRECTION('ref_axis',(0.479425538604204,0.,-0.877582561890372)) ;
#5462=DIRECTION('',(0.,1.,0.)) ;
#5463=DIRECTION('center_axis',(0.,-1.,0.)) ;
#5464=DIRECTION('ref_axis',(0.479425538604204,0.,-0.877582561890372)) ;
#5465=DIRECTION('center_axis',(0.877582561890372,0.,0.479425538604204)) ;
#5466=DIRECTION('ref_axis',(-0.479425538604204,0.,0.877582561890372)) ;
#5467=DIRECTION('center_axis',(0.,-1.,0.)) ;
#5468=DIRECTION('ref_axis',(0.,0.,1.)) ;
#5469=DIRECTION('center_axis',(0.,-1.,0.)) ;
#5470=DIRECTION('ref_axis',(0.479425538604204,0.,-0.877582561890372)) ;
#5471=DIRECTION('',(0.,1.,0.)) ;
#5472=DIRECTION('center_axis',(0.,-1.,0.)) ;
#5473=DIRECTION('ref_axis',(0.,0.,1.)) ;
#5474=DIRECTION('center_axis',(0.,-1.,0.)) ;
#5475=DIRECTION('ref_axis',(0.479425538604204,0.,-0.877582561890372)) ;
#5476=DIRECTION('',(0.339005049420894,0.707106781186865,-0.620544580563467)) ;
#6551=CARTESIAN_POINT('',(0.,0.,0.)) ;
#6552=CARTESIAN_POINT('Origin',(-37.5,-26.,11.443375673)) ;
#6553=CARTESIAN_POINT('',(-37.5,-26.,-8.55662432703)) ;
#6554=CARTESIAN_POINT('',(-37.5,-23.,-8.55662432703)) ;
#6555=CARTESIAN_POINT('',(-37.5,-24.5,-8.55662432703)) ;
#6556=CARTESIAN_POINT('',(-37.5,-26.,-11.443375673)) ;
#6557=CARTESIAN_POINT('',(-37.5,-26.,-10.)) ;
#6558=CARTESIAN_POINT('',(-37.5,-23.,-11.443375673)) ;
#6559=CARTESIAN_POINT('',(-37.5,-24.5,-11.443375673)) ;
#6560=CARTESIAN_POINT('',(-37.5,-23.,-10.)) ;
#6561=CARTESIAN_POINT('Origin',(-35.,-26.,-7.11324865405)) ;
#6562=CARTESIAN_POINT('',(-35.,-26.,-7.11324865405)) ;
#6563=CARTESIAN_POINT('',(-35.,-23.,-7.11324865405)) ;
#6564=CARTESIAN_POINT('',(-35.,-24.5,-7.11324865405)) ;
#6565=CARTESIAN_POINT('',(-36.25,-26.,-7.83493649054)) ;
#6566=CARTESIAN_POINT('',(-36.25,-23.,-7.83493649054)) ;
#6567=CARTESIAN_POINT('Origin',(-37.5,-26.,-11.443375673)) ;
#6568=CARTESIAN_POINT('',(-35.,-26.,-12.8867513459)) ;
#6569=CARTESIAN_POINT('',(-36.25,-26.,-12.1650635095)) ;
#6570=CARTESIAN_POINT('',(-35.,-23.,-12.8867513459)) ;
#6571=CARTESIAN_POINT('',(-35.,-24.5,-12.8867513459)) ;
#6572=CARTESIAN_POINT('',(-36.25,-23.,-12.1650635095)) ;
#6573=CARTESIAN_POINT('Origin',(-35.,-23.,10.)) ;
#6574=CARTESIAN_POINT('',(-32.5,-23.,-11.443375673)) ;
#6575=CARTESIAN_POINT('',(-33.75,-23.,-12.1650635095)) ;
#6576=CARTESIAN_POINT('',(-32.5,-23.,-8.55662432703)) ;
#6577=CARTESIAN_POINT('',(-32.5,-23.,-10.)) ;
#6578=CARTESIAN_POINT('',(-33.75,-23.,-7.83493649054)) ;
#6579=CARTESIAN_POINT('Origin',(-32.5,-26.,-8.55662432703)) ;
#6580=CARTESIAN_POINT('',(-32.5,-26.,-8.55662432703)) ;
#6581=CARTESIAN_POINT('',(-32.5,-24.5,-8.55662432703)) ;
#6582=CARTESIAN_POINT('',(-33.75,-26.,-7.83493649054)) ;
#6583=CARTESIAN_POINT('Origin',(-35.,-26.,-12.8867513459)) ;
#6584=CARTESIAN_POINT('',(-32.5,-26.,-11.443375673)) ;
#6585=CARTESIAN_POINT('',(-33.75,-26.,-12.1650635095)) ;
#6586=CARTESIAN_POINT('',(-32.5,-24.5,-11.443375673)) ;
#6587=CARTESIAN_POINT('Origin',(-32.5,-26.,8.55662432703)) ;
#6588=CARTESIAN_POINT('',(-32.5,-26.,-10.)) ;
#6589=CARTESIAN_POINT('Origin',(-35.,-26.,10.)) ;
#6590=CARTESIAN_POINT('',(-37.1094723699,-26.,-6.13863672768)) ;
#6591=CARTESIAN_POINT('Origin',(-35.,-26.,-10.)) ;
#6592=CARTESIAN_POINT('Origin',(-35.,-20.,5.)) ;
#6593=CARTESIAN_POINT('',(-37.397127693,-20.,-5.61208719055)) ;
#6594=CARTESIAN_POINT('Origin',(-35.,-20.,-10.)) ;
#6595=CARTESIAN_POINT('',(-36.5581330005,-20.,-7.14785667386)) ;
#6596=CARTESIAN_POINT('Origin',(-35.,-20.,-10.)) ;
#6597=CARTESIAN_POINT('Origin',(-35.,40.,7.5)) ;
#6598=CARTESIAN_POINT('',(-36.1985638465,40.,-7.80604359527)) ;
#6599=CARTESIAN_POINT('Origin',(-35.,40.,-10.)) ;
#6600=CARTESIAN_POINT('Origin',(-35.,-25.4,-10.)) ;
#6601=CARTESIAN_POINT('',(-37.397127693,-25.4,-5.61208719055)) ;
#6602=CARTESIAN_POINT('Origin',(-37.1094723698585,-25.4,-6.13863672768236)) ;
#6603=CARTESIAN_POINT('Origin',(-35.,-25.4,-10.)) ;
#6604=CARTESIAN_POINT('Origin',(-35.,7.,-10.)) ;
#6605=CARTESIAN_POINT('',(-37.397127693021,7.,-5.61208719054814)) ;
#6606=CARTESIAN_POINT('Origin',(-35.,-19.75,-10.)) ;
#6607=CARTESIAN_POINT('',(-36.4382766158,-19.75,-7.36725231433)) ;
#6608=CARTESIAN_POINT('Origin',(-36.5581330004637,-19.75,-7.14785667385629)) ;
#6609=CARTESIAN_POINT('Origin',(-35.,-19.75,-10.)) ;
#6610=CARTESIAN_POINT('Origin',(-35.,7.,-10.)) ;
#6611=CARTESIAN_POINT('',(-36.4382766158,39.5,-7.36725231433)) ;
#6612=CARTESIAN_POINT('',(-36.4382766158126,7.,-7.36725231432888)) ;
#6613=CARTESIAN_POINT('Origin',(-35.,39.5,-10.)) ;
#6614=CARTESIAN_POINT('Origin',(-35.,40.,-10.)) ;
#6615=CARTESIAN_POINT('',(-36.1985638465105,40.,-7.80604359527407)) ;
#6764=UNCERTAINTY_MEASURE_WITH_UNIT(LENGTH_MEASURE(0.01),#6780,
'DISTANCE_ACCURACY_VALUE',
'Maximum model space distance between geometric entities at asserted c
onnectivities') ;
#6767=UNCERTAINTY_MEASURE_WITH_UNIT(LENGTH_MEASURE(0.01),#6780,
'DISTANCE_ACCURACY_VALUE',
'Maximum model space distance between geometric entities at asserted c
onnectivities') ;
#6776=(
GEOMETRIC_REPRESENTATION_CONTEXT(3)
GLOBAL_UNCERTAINTY_ASSIGNED_CONTEXT((#6764))
GLOBAL_UNIT_ASSIGNED_CONTEXT((#6780,#6782,#6783))
REPRESENTATION_CONTEXT('','3D')
) ;
#6779=(
GEOMETRIC_REPRESENTATION_CONTEXT(3)
GLOBAL_UNCERTAINTY_ASSIGNED_CONTEXT((#6767))
GLOBAL_UNIT_ASSIGNED_CONTEXT((#6780,#6782,#6783))
REPRESENTATION_CONTEXT('','3D')
) ;
#6780=(
LENGTH_UNIT()
NAMED_UNIT(*)
SI_UNIT(.MILLI.,.METRE.)
) ;
#6782=(
NAMED_UNIT(*)
PLANE_ANGLE_UNIT()
SI_UNIT($,.RADIAN.)
) ;
#6783=(
NAMED_UNIT(*)
SI_UNIT($,.STERADIAN.)
SOLID_ANGLE_UNIT()
) ;
#6792=SHAPE_DEFINITION_REPRESENTATION(#6803,#6824) ;
#6803=PRODUCT_DEFINITION_SHAPE('',$,#6836) ;
#6824=SHAPE_REPRESENTATION('',(#4352),#6776) ;
#6827=PRODUCT_DEFINITION_CONTEXT('part definition',#6862,'design') ;
#6836=PRODUCT_DEFINITION('Clamp_Bolt_2','Clamp_Bolt_2',#6847,#6827) ;
#6847=PRODUCT_DEFINITION_FORMATION('',$,#6872) ;
#6862=APPLICATION_CONTEXT(
'Core Data for Automotive Mechanical Design Process') ;
#6863=PRODUCT_CONTEXT('part definition',#6862,'mechanical') ;
#6872=PRODUCT('Clamp_Bolt_2','Clamp_Bolt_2',$,(#6863)) ;
#6877=PRESENTATION_STYLE_ASSIGNMENT((#6880)) ;
#6880=SURFACE_STYLE_USAGE(.BOTH.,#6883) ;
#6883=SURFACE_SIDE_STYLE('',(#6886)) ;
#6886=SURFACE_STYLE_FILL_AREA(#6889) ;
#6889=FILL_AREA_STYLE('Opaque(203,203,203)',(#6892)) ;
#6892=FILL_AREA_STYLE_COLOUR('Opaque(203,203,203)',#6895) ;
#6895=COLOUR_RGB('Opaque(203,203,203)', 0.31764706, 0.68627451, 0.89019608) ;
ENDSEC;
END-ISO-10303-21;
